ISO-10303-21;
HEADER;
FILE_DESCRIPTION((''),'2;1');
FILE_NAME('SHELL_CLAMP_BOLT_M6x85.step','2026-10-01T22:05:39-07:00',(''),(''),'','','');
FILE_SCHEMA (('AUTOMOTIVE_DESIGN { 1 0 10303 214 3 1 1 }'));
ENDSEC;
DATA;
#10=MECHANICAL_DESIGN_GEOMETRIC_PRESENTATION_REPRESENTATION('',(#645),#24628);
#561=SHAPE_REPRESENTATION_RELATIONSHIP('SRR','None',#24836,#603) ;
#603=ADVANCED_BREP_SHAPE_REPRESENTATION('',(#684),#24626) ;
#645=STYLED_ITEM('',(#25030),#684) ;
#684=MANIFOLD_SOLID_BREP('SHELL_CLAMP_BOLT_M6x85',#13187) ;
#948=FACE_BOUND('',#4739,.T.) ;
#1799=LINE('',#24424,#2635) ;
#1800=LINE('',#24430,#2636) ;
#1801=LINE('',#24432,#2637) ;
#1802=LINE('',#24434,#2638) ;
#1803=LINE('',#24435,#2639) ;
#1804=LINE('',#24439,#2640) ;
#1805=LINE('',#24441,#2641) ;
#1806=LINE('',#24443,#2642) ;
#1807=LINE('',#24444,#2643) ;
#1808=LINE('',#24447,#2644) ;
#1809=LINE('',#24448,#2645) ;
#1810=LINE('',#24450,#2646) ;
#1811=LINE('',#24451,#2647) ;
#1812=LINE('',#24454,#2648) ;
#1813=LINE('',#24455,#2649) ;
#1814=LINE('',#24458,#2650) ;
#1815=LINE('',#24459,#2651) ;
#1816=LINE('',#24461,#2652) ;
#1817=LINE('',#24463,#2653) ;
#2635=VECTOR('',#19574,0.3) ;
#2636=VECTOR('',#19581,1.) ;
#2637=VECTOR('',#19582,1.) ;
#2638=VECTOR('',#19583,1.) ;
#2639=VECTOR('',#19584,1.) ;
#2640=VECTOR('',#19587,1.) ;
#2641=VECTOR('',#19588,1.) ;
#2642=VECTOR('',#19589,1.) ;
#2643=VECTOR('',#19590,1.) ;
#2644=VECTOR('',#19593,1.) ;
#2645=VECTOR('',#19594,1.) ;
#2646=VECTOR('',#19595,1.) ;
#2647=VECTOR('',#19596,1.) ;
#2648=VECTOR('',#19599,1.) ;
#2649=VECTOR('',#19600,1.) ;
#2650=VECTOR('',#19603,1.) ;
#2651=VECTOR('',#19604,1.) ;
#2652=VECTOR('',#19607,1.) ;
#2653=VECTOR('',#19610,1.) ;
#2950=CYLINDRICAL_SURFACE('',#15343,0.3) ;
#3700=FACE_OUTER_BOUND('',#4729,.T.) ;
#3701=FACE_OUTER_BOUND('',#4730,.T.) ;
#3702=FACE_OUTER_BOUND('',#4731,.T.) ;
#3703=FACE_OUTER_BOUND('',#4732,.T.) ;
#3704=FACE_OUTER_BOUND('',#4733,.T.) ;
#3705=FACE_OUTER_BOUND('',#4734,.T.) ;
#3706=FACE_OUTER_BOUND('',#4735,.T.) ;
#3707=FACE_OUTER_BOUND('',#4736,.T.) ;
#3708=FACE_OUTER_BOUND('',#4737,.T.) ;
#3709=FACE_OUTER_BOUND('',#4738,.T.) ;
#4729=EDGE_LOOP('',(#11911,#11912,#11913,#11914)) ;
#4730=EDGE_LOOP('',(#11915)) ;
#4731=EDGE_LOOP('',(#11916,#11917,#11918,#11919)) ;
#4732=EDGE_LOOP('',(#11920,#11921,#11922,#11923)) ;
#4733=EDGE_LOOP('',(#11924,#11925,#11926,#11927,#11928,#11929)) ;
#4734=EDGE_LOOP('',(#11930,#11931,#11932,#11933)) ;
#4735=EDGE_LOOP('',(#11934,#11935,#11936,#11937)) ;
#4736=EDGE_LOOP('',(#11938,#11939,#11940,#11941)) ;
#4737=EDGE_LOOP('',(#11942,#11943,#11944,#11945)) ;
#4738=EDGE_LOOP('',(#11946,#11947,#11948,#11949,#11950,#11951)) ;
#4739=EDGE_LOOP('',(#11952)) ;
#5533=CIRCLE('',#15344,0.3) ;
#5534=CIRCLE('',#15345,0.3) ;
#6705=VERTEX_POINT('',#24421) ;
#6706=VERTEX_POINT('',#24423) ;
#6707=VERTEX_POINT('',#24428) ;
#6708=VERTEX_POINT('',#24429) ;
#6709=VERTEX_POINT('',#24431) ;
#6710=VERTEX_POINT('',#24433) ;
#6711=VERTEX_POINT('',#24437) ;
#6712=VERTEX_POINT('',#24438) ;
#6713=VERTEX_POINT('',#24440) ;
#6714=VERTEX_POINT('',#24442) ;
#6715=VERTEX_POINT('',#24446) ;
#6716=VERTEX_POINT('',#24449) ;
#6717=VERTEX_POINT('',#24453) ;
#6718=VERTEX_POINT('',#24457) ;
#8445=EDGE_CURVE('',#6705,#6705,#5533,.T.) ;
#8446=EDGE_CURVE('',#6705,#6706,#1799,.T.) ;
#8447=EDGE_CURVE('',#6706,#6706,#5534,.T.) ;
#8448=EDGE_CURVE('',#6707,#6708,#1800,.T.) ;
#8449=EDGE_CURVE('',#6707,#6709,#1801,.T.) ;
#8450=EDGE_CURVE('',#6710,#6709,#1802,.T.) ;
#8451=EDGE_CURVE('',#6710,#6708,#1803,.T.) ;
#8452=EDGE_CURVE('',#6711,#6712,#1804,.T.) ;
#8453=EDGE_CURVE('',#6711,#6713,#1805,.T.) ;
#8454=EDGE_CURVE('',#6714,#6713,#1806,.T.) ;
#8455=EDGE_CURVE('',#6714,#6712,#1807,.T.) ;
#8456=EDGE_CURVE('',#6715,#6707,#1808,.T.) ;
#8457=EDGE_CURVE('',#6713,#6715,#1809,.T.) ;
#8458=EDGE_CURVE('',#6716,#6711,#1810,.T.) ;
#8459=EDGE_CURVE('',#6709,#6716,#1811,.T.) ;
#8460=EDGE_CURVE('',#6715,#6717,#1812,.T.) ;
#8461=EDGE_CURVE('',#6708,#6717,#1813,.T.) ;
#8462=EDGE_CURVE('',#6716,#6718,#1814,.T.) ;
#8463=EDGE_CURVE('',#6712,#6718,#1815,.T.) ;
#8464=EDGE_CURVE('',#6717,#6714,#1816,.T.) ;
#8465=EDGE_CURVE('',#6718,#6710,#1817,.T.) ;
#11911=ORIENTED_EDGE('',*,*,#8445,.F.) ;
#11912=ORIENTED_EDGE('',*,*,#8446,.T.) ;
#11913=ORIENTED_EDGE('',*,*,#8447,.F.) ;
#11914=ORIENTED_EDGE('',*,*,#8446,.F.) ;
#11915=ORIENTED_EDGE('',*,*,#8445,.T.) ;
#11916=ORIENTED_EDGE('',*,*,#8448,.F.) ;
#11917=ORIENTED_EDGE('',*,*,#8449,.T.) ;
#11918=ORIENTED_EDGE('',*,*,#8450,.F.) ;
#11919=ORIENTED_EDGE('',*,*,#8451,.T.) ;
#11920=ORIENTED_EDGE('',*,*,#8452,.F.) ;
#11921=ORIENTED_EDGE('',*,*,#8453,.T.) ;
#11922=ORIENTED_EDGE('',*,*,#8454,.F.) ;
#11923=ORIENTED_EDGE('',*,*,#8455,.T.) ;
#11924=ORIENTED_EDGE('',*,*,#8449,.F.) ;
#11925=ORIENTED_EDGE('',*,*,#8456,.F.) ;
#11926=ORIENTED_EDGE('',*,*,#8457,.F.) ;
#11927=ORIENTED_EDGE('',*,*,#8453,.F.) ;
#11928=ORIENTED_EDGE('',*,*,#8458,.F.) ;
#11929=ORIENTED_EDGE('',*,*,#8459,.F.) ;
#11930=ORIENTED_EDGE('',*,*,#8460,.F.) ;
#11931=ORIENTED_EDGE('',*,*,#8456,.T.) ;
#11932=ORIENTED_EDGE('',*,*,#8448,.T.) ;
#11933=ORIENTED_EDGE('',*,*,#8461,.T.) ;
#11934=ORIENTED_EDGE('',*,*,#8462,.F.) ;
#11935=ORIENTED_EDGE('',*,*,#8458,.T.) ;
#11936=ORIENTED_EDGE('',*,*,#8452,.T.) ;
#11937=ORIENTED_EDGE('',*,*,#8463,.T.) ;
#11938=ORIENTED_EDGE('',*,*,#8460,.T.) ;
#11939=ORIENTED_EDGE('',*,*,#8464,.T.) ;
#11940=ORIENTED_EDGE('',*,*,#8454,.T.) ;
#11941=ORIENTED_EDGE('',*,*,#8457,.T.) ;
#11942=ORIENTED_EDGE('',*,*,#8450,.T.) ;
#11943=ORIENTED_EDGE('',*,*,#8459,.T.) ;
#11944=ORIENTED_EDGE('',*,*,#8462,.T.) ;
#11945=ORIENTED_EDGE('',*,*,#8465,.T.) ;
#11946=ORIENTED_EDGE('',*,*,#8451,.F.) ;
#11947=ORIENTED_EDGE('',*,*,#8465,.F.) ;
#11948=ORIENTED_EDGE('',*,*,#8463,.F.) ;
#11949=ORIENTED_EDGE('',*,*,#8455,.F.) ;
#11950=ORIENTED_EDGE('',*,*,#8464,.F.) ;
#11951=ORIENTED_EDGE('',*,*,#8461,.F.) ;
#11952=ORIENTED_EDGE('',*,*,#8447,.T.) ;
#12330=PLANE('',#15346) ;
#12331=PLANE('',#15347) ;
#12332=PLANE('',#15348) ;
#12333=PLANE('',#15349) ;
#12334=PLANE('',#15350) ;
#12335=PLANE('',#15351) ;
#12336=PLANE('',#15352) ;
#12337=PLANE('',#15353) ;
#12338=PLANE('',#15354) ;
#13095=ADVANCED_FACE('',(#3700),#2950,.T.) ;
#13096=ADVANCED_FACE('',(#3701),#12330,.T.) ;
#13097=ADVANCED_FACE('',(#3702),#12331,.F.) ;
#13098=ADVANCED_FACE('',(#3703),#12332,.F.) ;
#13099=ADVANCED_FACE('',(#3704),#12333,.T.) ;
#13100=ADVANCED_FACE('',(#3705),#12334,.F.) ;
#13101=ADVANCED_FACE('',(#3706),#12335,.F.) ;
#13102=ADVANCED_FACE('',(#3707),#12336,.F.) ;
#13103=ADVANCED_FACE('',(#3708),#12337,.F.) ;
#13104=ADVANCED_FACE('',(#3709,#948),#12338,.T.) ;
#13187=CLOSED_SHELL('',(#13095,#13096,#13097,#13098,#13099,#13100,#13101,
#13102,#13103,#13104)) ;
#15342=AXIS2_PLACEMENT_3D('',#24419,#19568,#19569) ;
#15343=AXIS2_PLACEMENT_3D('',#24420,#19570,#19571) ;
#15344=AXIS2_PLACEMENT_3D('',#24422,#19572,#19573) ;
#15345=AXIS2_PLACEMENT_3D('',#24425,#19575,#19576) ;
#15346=AXIS2_PLACEMENT_3D('',#24426,#19577,#19578) ;
#15347=AXIS2_PLACEMENT_3D('',#24427,#19579,#19580) ;
#15348=AXIS2_PLACEMENT_3D('',#24436,#19585,#19586) ;
#15349=AXIS2_PLACEMENT_3D('',#24445,#19591,#19592) ;
#15350=AXIS2_PLACEMENT_3D('',#24452,#19597,#19598) ;
#15351=AXIS2_PLACEMENT_3D('',#24456,#19601,#19602) ;
#15352=AXIS2_PLACEMENT_3D('',#24460,#19605,#19606) ;
#15353=AXIS2_PLACEMENT_3D('',#24462,#19608,#19609) ;
#15354=AXIS2_PLACEMENT_3D('',#24464,#19611,#19612) ;
#19568=DIRECTION('axis',(0.,0.,1.)) ;
#19569=DIRECTION('refdir',(1.,0.,0.)) ;
#19570=DIRECTION('center_axis',(0.,-1.,0.)) ;
#19571=DIRECTION('ref_axis',(1.,0.,0.)) ;
#19572=DIRECTION('center_axis',(0.,-1.,0.)) ;
#19573=DIRECTION('ref_axis',(1.,0.,0.)) ;
#19574=DIRECTION('',(0.,1.,0.)) ;
#19575=DIRECTION('center_axis',(0.,1.,0.)) ;
#19576=DIRECTION('ref_axis',(1.,0.,0.)) ;
#19577=DIRECTION('center_axis',(0.,-1.,0.)) ;
#19578=DIRECTION('ref_axis',(1.,0.,0.)) ;
#19579=DIRECTION('center_axis',(-0.5,0.,0.866025403784439)) ;
#19580=DIRECTION('ref_axis',(-0.866025403784439,0.,-0.5)) ;
#19581=DIRECTION('',(0.,-1.,0.)) ;
#19582=DIRECTION('',(0.866025403784439,0.,0.5)) ;
#19583=DIRECTION('',(0.,1.,0.)) ;
#19584=DIRECTION('',(-0.866025403784439,0.,-0.5)) ;
#19585=DIRECTION('center_axis',(0.5,0.,-0.866025403784439)) ;
#19586=DIRECTION('ref_axis',(0.866025403784439,0.,0.5)) ;
#19587=DIRECTION('',(0.,-1.,0.)) ;
#19588=DIRECTION('',(-0.866025403784439,0.,-0.5)) ;
#19589=DIRECTION('',(0.,1.,0.)) ;
#19590=DIRECTION('',(0.866025403784439,0.,0.5)) ;
#19591=DIRECTION('center_axis',(0.,1.,0.)) ;
#19592=DIRECTION('ref_axis',(-1.,0.,0.)) ;
#19593=DIRECTION('',(0.866025403784439,0.,-0.5)) ;
#19594=DIRECTION('',(0.,0.,-1.)) ;
#19595=DIRECTION('',(-0.866025403784439,0.,0.5)) ;
#19596=DIRECTION('',(0.,0.,1.)) ;
#19597=DIRECTION('center_axis',(0.5,0.,0.866025403784439)) ;
#19598=DIRECTION('ref_axis',(-0.866025403784439,0.,0.5)) ;
#19599=DIRECTION('',(0.,-1.,0.)) ;
#19600=DIRECTION('',(-0.866025403784439,0.,0.5)) ;
#19601=DIRECTION('center_axis',(-0.5,0.,-0.866025403784439)) ;
#19602=DIRECTION('ref_axis',(0.866025403784439,0.,-0.5)) ;
#19603=DIRECTION('',(0.,-1.,0.)) ;
#19604=DIRECTION('',(0.866025403784439,0.,-0.5)) ;
#19605=DIRECTION('center_axis',(1.,0.,0.)) ;
#19606=DIRECTION('ref_axis',(0.,0.,1.)) ;
#19607=DIRECTION('',(0.,0.,1.)) ;
#19608=DIRECTION('center_axis',(-1.,0.,0.)) ;
#19609=DIRECTION('ref_axis',(0.,0.,-1.)) ;
#19610=DIRECTION('',(0.,0.,-1.)) ;
#19611=DIRECTION('center_axis',(0.,-1.,0.)) ;
#19612=DIRECTION('ref_axis',(1.,0.,0.)) ;
#24419=CARTESIAN_POINT('',(0.,0.,0.)) ;
#24420=CARTESIAN_POINT('Origin',(0.,-4.25,0.)) ;
#24421=CARTESIAN_POINT('',(-0.3,-8.5,-3.67394039744206E-17)) ;
#24422=CARTESIAN_POINT('Origin',(0.,-8.5,0.)) ;
#24423=CARTESIAN_POINT('',(-0.3,0.,-3.67394039744206E-17)) ;
#24424=CARTESIAN_POINT('',(-0.3,-4.25,-3.67394039744206E-17)) ;
#24425=CARTESIAN_POINT('Origin',(0.,0.,0.)) ;
#24426=CARTESIAN_POINT('Origin',(0.,-8.5,0.)) ;
#24427=CARTESIAN_POINT('Origin',(0.25,0.2,-0.433012701892219)) ;
#24428=CARTESIAN_POINT('',(-8.32667268468867E-17,0.4,-0.577350269189626)) ;
#24429=CARTESIAN_POINT('',(-8.32667268468867E-17,0.,-0.577350269189626)) ;
#24430=CARTESIAN_POINT('',(-8.32667268468867E-17,0.2,-0.577350269189626)) ;
#24431=CARTESIAN_POINT('',(0.5,0.4,-0.288675134594813)) ;
#24432=CARTESIAN_POINT('',(0.25,0.4,-0.433012701892219)) ;
#24433=CARTESIAN_POINT('',(0.5,0.,-0.288675134594813)) ;
#24434=CARTESIAN_POINT('',(0.5,0.2,-0.288675134594813)) ;
#24435=CARTESIAN_POINT('',(0.25,0.,-0.433012701892219)) ;
#24436=CARTESIAN_POINT('Origin',(-0.25,0.2,0.433012701892219)) ;
#24437=CARTESIAN_POINT('',(8.32667268468867E-17,0.4,0.577350269189626)) ;
#24438=CARTESIAN_POINT('',(8.32667268468867E-17,0.,0.577350269189626)) ;
#24439=CARTESIAN_POINT('',(8.32667268468867E-17,0.2,0.577350269189626)) ;
#24440=CARTESIAN_POINT('',(-0.5,0.4,0.288675134594813)) ;
#24441=CARTESIAN_POINT('',(-0.25,0.4,0.433012701892219)) ;
#24442=CARTESIAN_POINT('',(-0.5,0.,0.288675134594813)) ;
#24443=CARTESIAN_POINT('',(-0.5,0.2,0.288675134594813)) ;
#24444=CARTESIAN_POINT('',(-0.25,0.,0.433012701892219)) ;
#24445=CARTESIAN_POINT('Origin',(0.,0.4,0.)) ;
#24446=CARTESIAN_POINT('',(-0.5,0.4,-0.288675134594813)) ;
#24447=CARTESIAN_POINT('',(-0.25,0.4,-0.433012701892219)) ;
#24448=CARTESIAN_POINT('',(-0.5,0.4,0.)) ;
#24449=CARTESIAN_POINT('',(0.5,0.4,0.288675134594813)) ;
#24450=CARTESIAN_POINT('',(0.25,0.4,0.433012701892219)) ;
#24451=CARTESIAN_POINT('',(0.5,0.4,0.)) ;
#24452=CARTESIAN_POINT('Origin',(-0.25,0.2,-0.433012701892219)) ;
#24453=CARTESIAN_POINT('',(-0.5,0.,-0.288675134594813)) ;
#24454=CARTESIAN_POINT('',(-0.5,0.2,-0.288675134594813)) ;
#24455=CARTESIAN_POINT('',(-0.25,0.,-0.433012701892219)) ;
#24456=CARTESIAN_POINT('Origin',(0.25,0.2,0.433012701892219)) ;
#24457=CARTESIAN_POINT('',(0.5,0.,0.288675134594813)) ;
#24458=CARTESIAN_POINT('',(0.5,0.2,0.288675134594813)) ;
#24459=CARTESIAN_POINT('',(0.25,0.,0.433012701892219)) ;
#24460=CARTESIAN_POINT('Origin',(-0.5,0.2,0.)) ;
#24461=CARTESIAN_POINT('',(-0.5,0.,0.)) ;
#24462=CARTESIAN_POINT('Origin',(0.5,0.2,0.)) ;
#24463=CARTESIAN_POINT('',(0.5,0.,0.)) ;
#24464=CARTESIAN_POINT('Origin',(0.,0.,0.)) ;
#24578=UNCERTAINTY_MEASURE_WITH_UNIT(LENGTH_MEASURE(0.001),#24629,
'DISTANCE_ACCURACY_VALUE',
'Maximum model space distance between geometric entities at asserted c
onnectivities') ;
#24580=UNCERTAINTY_MEASURE_WITH_UNIT(LENGTH_MEASURE(0.001),#24629,
'DISTANCE_ACCURACY_VALUE',
'Maximum model space distance between geometric entities at asserted c
onnectivities') ;
#24626=(
GEOMETRIC_REPRESENTATION_CONTEXT(3)
GLOBAL_UNCERTAINTY_ASSIGNED_CONTEXT((#24578))
GLOBAL_UNIT_ASSIGNED_CONTEXT((#24629,#24631,#24632))
REPRESENTATION_CONTEXT('','3D')
) ;
#24628=(
GEOMETRIC_REPRESENTATION_CONTEXT(3)
GLOBAL_UNCERTAINTY_ASSIGNED_CONTEXT((#24580))
GLOBAL_UNIT_ASSIGNED_CONTEXT((#24629,#24631,#24632))
REPRESENTATION_CONTEXT('','3D')
) ;
#24629=(
LENGTH_UNIT()
NAMED_UNIT(*)
SI_UNIT(.CENTI.,.METRE.)
) ;
#24631=(
NAMED_UNIT(*)
PLANE_ANGLE_UNIT()
SI_UNIT($,.RADIAN.)
) ;
#24632=(
NAMED_UNIT(*)
SI_UNIT($,.STERADIAN.)
SOLID_ANGLE_UNIT()
) ;
#24678=SHAPE_DEFINITION_REPRESENTATION(#24766,#24836) ;
#24766=PRODUCT_DEFINITION_SHAPE('',$,#24884) ;
#24836=SHAPE_REPRESENTATION('',(#15342),#24626) ;
#24838=PRODUCT_DEFINITION_CONTEXT('part definition',#24981,'design') ;
#24884=PRODUCT_DEFINITION('SHELL_CLAMP_BOLT_M6x85',
'SHELL_CLAMP_BOLT_M6x85',#24931,#24838) ;
#24931=PRODUCT_DEFINITION_FORMATION('',$,#25028) ;
#24981=APPLICATION_CONTEXT(
'Core Data for Automotive Mechanical Design Process') ;
#24982=PRODUCT_CONTEXT('part definition',#24981,'mechanical') ;
#25028=PRODUCT('SHELL_CLAMP_BOLT_M6x85','SHELL_CLAMP_BOLT_M6x85',$,(#24982)) ;
#25030=PRESENTATION_STYLE_ASSIGNMENT((#25040)) ;
#25040=SURFACE_STYLE_USAGE(.BOTH.,#25050) ;
#25050=SURFACE_SIDE_STYLE('',(#25060)) ;
#25060=SURFACE_STYLE_FILL_AREA(#25070) ;
#25070=FILL_AREA_STYLE('Steel - Satin',(#25080)) ;
#25080=FILL_AREA_STYLE_COLOUR('Steel - Satin',#25090) ;
#25090=COLOUR_RGB('Steel - Satin', 0.66274510, 0.83137255, 0.94901961) ;
ENDSEC;
END-ISO-10303-21;
